ISO-10303-21;
HEADER;
/* Generated by software containing ST-Developer
 * from STEP Tools, Inc. (www.steptools.com) 
 */

FILE_DESCRIPTION(
/* description */ (''),
/* implementation_level */ '2;1');

FILE_NAME(
/* name */ 'Right_Block.step',
/* time_stamp */ '2026-10-23T22:29:29+06:00',
/* author */ (''),
/* organization */ (''),
/* preprocessor_version */ 'ST-DEVELOPER v20.2',
/* originating_system */ 'Autodesk Translation Framework v15.15.0.0',
/* authorisation */ '');

FILE_SCHEMA (('AUTOMOTIVE_DESIGN { 1 0 10303 214 3 1 1 }'));
ENDSEC;

DATA;
#10=MECHANICAL_DESIGN_GEOMETRIC_PRESENTATION_REPRESENTATION('',(#79),#7047);
#59=SHAPE_REPRESENTATION_RELATIONSHIP('SRR','None',#7092,#69);
#69=ADVANCED_BREP_SHAPE_REPRESENTATION('',(#92),#7044);
#79=STYLED_ITEM('',(#7177),#92);
#92=MANIFOLD_SOLID_BREP('Right_Block',#3404);
#121=FACE_BOUND('',#626,.T.);
#122=FACE_BOUND('',#639,.T.);
#229=PLANE('',#3828);
#230=PLANE('',#3829);
#231=PLANE('',#3830);
#232=PLANE('',#3831);
#233=PLANE('',#3832);
#234=PLANE('',#3833);
#235=PLANE('',#3834);
#236=PLANE('',#3838);
#237=PLANE('',#3841);
#238=PLANE('',#3843);
#239=PLANE('',#3847);
#240=PLANE('',#3848);
#241=PLANE('',#3849);
#242=PLANE('',#3850);
#243=PLANE('',#3853);
#244=PLANE('',#3854);
#245=PLANE('',#3855);
#246=PLANE('',#3858);
#247=PLANE('',#3859);
#413=FACE_OUTER_BOUND('',#616,.T.);
#414=FACE_OUTER_BOUND('',#617,.T.);
#415=FACE_OUTER_BOUND('',#618,.T.);
#416=FACE_OUTER_BOUND('',#619,.T.);
#417=FACE_OUTER_BOUND('',#620,.T.);
#418=FACE_OUTER_BOUND('',#621,.T.);
#419=FACE_OUTER_BOUND('',#622,.T.);
#420=FACE_OUTER_BOUND('',#623,.T.);
#421=FACE_OUTER_BOUND('',#624,.T.);
#422=FACE_OUTER_BOUND('',#625,.T.);
#423=FACE_OUTER_BOUND('',#627,.T.);
#424=FACE_OUTER_BOUND('',#628,.T.);
#425=FACE_OUTER_BOUND('',#629,.T.);
#426=FACE_OUTER_BOUND('',#630,.T.);
#427=FACE_OUTER_BOUND('',#631,.T.);
#428=FACE_OUTER_BOUND('',#632,.T.);
#429=FACE_OUTER_BOUND('',#633,.T.);
#430=FACE_OUTER_BOUND('',#634,.T.);
#431=FACE_OUTER_BOUND('',#635,.T.);
#432=FACE_OUTER_BOUND('',#636,.T.);
#433=FACE_OUTER_BOUND('',#637,.T.);
#434=FACE_OUTER_BOUND('',#638,.T.);
#435=FACE_OUTER_BOUND('',#640,.T.);
#616=EDGE_LOOP('',(#2969,#2970,#2971,#2972));
#617=EDGE_LOOP('',(#2973,#2974,#2975,#2976));
#618=EDGE_LOOP('',(#2977,#2978,#2979,#2980));
#619=EDGE_LOOP('',(#2981,#2982,#2983,#2984));
#620=EDGE_LOOP('',(#2985,#2986,#2987,#2988,#2989,#2990,#2991,#2992));
#621=EDGE_LOOP('',(#2993,#2994,#2995,#2996));
#622=EDGE_LOOP('',(#2997,#2998,#2999,#3000));
#623=EDGE_LOOP('',(#3001,#3002,#3003,#3004));
#624=EDGE_LOOP('',(#3005,#3006,#3007,#3008,#3009,#3010,#3011,#3012,#3013,
#3014,#3015,#3016,#3017,#3018,#3019,#3020));
#625=EDGE_LOOP('',(#3021,#3022,#3023,#3024));
#626=EDGE_LOOP('',(#3025));
#627=EDGE_LOOP('',(#3026,#3027,#3028,#3029,#3030,#3031));
#628=EDGE_LOOP('',(#3032,#3033,#3034,#3035,#3036,#3037));
#629=EDGE_LOOP('',(#3038,#3039,#3040,#3041));
#630=EDGE_LOOP('',(#3042,#3043,#3044,#3045));
#631=EDGE_LOOP('',(#3046,#3047,#3048,#3049,#3050));
#632=EDGE_LOOP('',(#3051,#3052,#3053,#3054));
#633=EDGE_LOOP('',(#3055,#3056,#3057,#3058));
#634=EDGE_LOOP('',(#3059,#3060,#3061,#3062));
#635=EDGE_LOOP('',(#3063,#3064,#3065,#3066));
#636=EDGE_LOOP('',(#3067,#3068,#3069,#3070));
#637=EDGE_LOOP('',(#3071,#3072,#3073,#3074));
#638=EDGE_LOOP('',(#3075,#3076,#3077,#3078));
#639=EDGE_LOOP('',(#3079));
#640=EDGE_LOOP('',(#3080,#3081,#3082,#3083,#3084,#3085,#3086,#3087,#3088,
#3089,#3090,#3091,#3092,#3093,#3094));
#784=CIRCLE('',#3836,4.99999999999999);
#785=CIRCLE('',#3837,4.99999999999999);
#786=CIRCLE('',#3839,4.99999999999999);
#787=CIRCLE('',#3840,4.99999999999999);
#788=CIRCLE('',#3842,2.5);
#789=CIRCLE('',#3845,4.99999999999999);
#790=CIRCLE('',#3846,4.99999999999999);
#791=CIRCLE('',#3852,4.99999999999999);
#792=CIRCLE('',#3857,2.5);
#1031=LINE('',#5936,#1325);
#1032=LINE('',#5938,#1326);
#1033=LINE('',#5940,#1327);
#1034=LINE('',#5941,#1328);
#1035=LINE('',#5944,#1329);
#1036=LINE('',#5946,#1330);
#1037=LINE('',#5947,#1331);
#1038=LINE('',#5950,#1332);
#1039=LINE('',#5952,#1333);
#1040=LINE('',#5953,#1334);
#1041=LINE('',#5955,#1335);
#1042=LINE('',#5958,#1336);
#1043=LINE('',#5960,#1337);
#1044=LINE('',#5962,#1338);
#1045=LINE('',#5964,#1339);
#1046=LINE('',#5965,#1340);
#1047=LINE('',#5969,#1341);
#1048=LINE('',#5971,#1342);
#1049=LINE('',#5973,#1343);
#1050=LINE('',#5974,#1344);
#1051=LINE('',#5977,#1345);
#1052=LINE('',#5979,#1346);
#1053=LINE('',#5980,#1347);
#1054=LINE('',#5985,#1348);
#1055=LINE('',#5989,#1349);
#1056=LINE('',#5993,#1350);
#1057=LINE('',#5995,#1351);
#1058=LINE('',#5997,#1352);
#1059=LINE('',#5999,#1353);
#1060=LINE('',#6001,#1354);
#1061=LINE('',#6004,#1355);
#1062=LINE('',#6005,#1356);
#1063=LINE('',#6010,#1357);
#1064=LINE('',#6012,#1358);
#1065=LINE('',#6014,#1359);
#1066=LINE('',#6016,#1360);
#1067=LINE('',#6017,#1361);
#1068=LINE('',#6021,#1362);
#1069=LINE('',#6027,#1363);
#1070=LINE('',#6029,#1364);
#1071=LINE('',#6031,#1365);
#1072=LINE('',#6032,#1366);
#1073=LINE('',#6034,#1367);
#1074=LINE('',#6035,#1368);
#1075=LINE('',#6037,#1369);
#1076=LINE('',#6039,#1370);
#1077=LINE('',#6042,#1371);
#1078=LINE('',#6046,#1372);
#1079=LINE('',#6048,#1373);
#1080=LINE('',#6049,#1374);
#1081=LINE('',#6051,#1375);
#1082=LINE('',#6053,#1376);
#1083=LINE('',#6057,#1377);
#1084=LINE('',#6059,#1378);
#1325=VECTOR('',#4718,10.);
#1326=VECTOR('',#4719,10.);
#1327=VECTOR('',#4720,10.);
#1328=VECTOR('',#4721,10.);
#1329=VECTOR('',#4724,10.);
#1330=VECTOR('',#4725,10.);
#1331=VECTOR('',#4726,10.);
#1332=VECTOR('',#4729,10.);
#1333=VECTOR('',#4730,10.);
#1334=VECTOR('',#4731,10.);
#1335=VECTOR('',#4734,10.);
#1336=VECTOR('',#4737,10.);
#1337=VECTOR('',#4738,10.);
#1338=VECTOR('',#4739,10.);
#1339=VECTOR('',#4740,10.);
#1340=VECTOR('',#4741,10.);
#1341=VECTOR('',#4744,10.);
#1342=VECTOR('',#4745,10.);
#1343=VECTOR('',#4746,10.);
#1344=VECTOR('',#4747,10.);
#1345=VECTOR('',#4750,10.);
#1346=VECTOR('',#4751,10.);
#1347=VECTOR('',#4752,10.);
#1348=VECTOR('',#4757,10.);
#1349=VECTOR('',#4762,10.);
#1350=VECTOR('',#4765,10.);
#1351=VECTOR('',#4766,10.);
#1352=VECTOR('',#4767,10.);
#1353=VECTOR('',#4768,10.);
#1354=VECTOR('',#4771,10.);
#1355=VECTOR('',#4774,10.);
#1356=VECTOR('',#4775,10.);
#1357=VECTOR('',#4780,10.);
#1358=VECTOR('',#4781,10.);
#1359=VECTOR('',#4782,10.);
#1360=VECTOR('',#4783,10.);
#1361=VECTOR('',#4784,10.);
#1362=VECTOR('',#4787,10.);
#1363=VECTOR('',#4794,10.);
#1364=VECTOR('',#4795,10.);
#1365=VECTOR('',#4796,10.);
#1366=VECTOR('',#4797,10.);
#1367=VECTOR('',#4800,10.);
#1368=VECTOR('',#4801,10.);
#1369=VECTOR('',#4804,10.);
#1370=VECTOR('',#4807,10.);
#1371=VECTOR('',#4810,10.);
#1372=VECTOR('',#4815,10.);
#1373=VECTOR('',#4816,10.);
#1374=VECTOR('',#4817,10.);
#1375=VECTOR('',#4820,10.);
#1376=VECTOR('',#4823,10.);
#1377=VECTOR('',#4828,2.5);
#1378=VECTOR('',#4831,10.);
#1677=VERTEX_POINT('',#5934);
#1678=VERTEX_POINT('',#5935);
#1679=VERTEX_POINT('',#5937);
#1680=VERTEX_POINT('',#5939);
#1681=VERTEX_POINT('',#5943);
#1682=VERTEX_POINT('',#5945);
#1683=VERTEX_POINT('',#5949);
#1684=VERTEX_POINT('',#5951);
#1685=VERTEX_POINT('',#5957);
#1686=VERTEX_POINT('',#5959);
#1687=VERTEX_POINT('',#5961);
#1688=VERTEX_POINT('',#5963);
#1689=VERTEX_POINT('',#5967);
#1690=VERTEX_POINT('',#5968);
#1691=VERTEX_POINT('',#5970);
#1692=VERTEX_POINT('',#5972);
#1693=VERTEX_POINT('',#5976);
#1694=VERTEX_POINT('',#5978);
#1695=VERTEX_POINT('',#5982);
#1696=VERTEX_POINT('',#5984);
#1697=VERTEX_POINT('',#5988);
#1698=VERTEX_POINT('',#5990);
#1699=VERTEX_POINT('',#5992);
#1700=VERTEX_POINT('',#5994);
#1701=VERTEX_POINT('',#5996);
#1702=VERTEX_POINT('',#5998);
#1703=VERTEX_POINT('',#6003);
#1704=VERTEX_POINT('',#6006);
#1705=VERTEX_POINT('',#6009);
#1706=VERTEX_POINT('',#6011);
#1707=VERTEX_POINT('',#6013);
#1708=VERTEX_POINT('',#6015);
#1709=VERTEX_POINT('',#6019);
#1710=VERTEX_POINT('',#6020);
#1711=VERTEX_POINT('',#6025);
#1712=VERTEX_POINT('',#6026);
#1713=VERTEX_POINT('',#6028);
#1714=VERTEX_POINT('',#6030);
#1715=VERTEX_POINT('',#6041);
#1716=VERTEX_POINT('',#6045);
#1717=VERTEX_POINT('',#6047);
#1718=VERTEX_POINT('',#6055);
#2119=EDGE_CURVE('',#1677,#1678,#1031,.T.);
#2120=EDGE_CURVE('',#1677,#1679,#1032,.T.);
#2121=EDGE_CURVE('',#1679,#1680,#1033,.T.);
#2122=EDGE_CURVE('',#1678,#1680,#1034,.T.);
#2123=EDGE_CURVE('',#1681,#1677,#1035,.T.);
#2124=EDGE_CURVE('',#1681,#1682,#1036,.T.);
#2125=EDGE_CURVE('',#1682,#1679,#1037,.T.);
#2126=EDGE_CURVE('',#1683,#1681,#1038,.T.);
#2127=EDGE_CURVE('',#1683,#1684,#1039,.T.);
#2128=EDGE_CURVE('',#1684,#1682,#1040,.T.);
#2129=EDGE_CURVE('',#1680,#1684,#1041,.T.);
#2130=EDGE_CURVE('',#1685,#1678,#1042,.T.);
#2131=EDGE_CURVE('',#1685,#1686,#1043,.T.);
#2132=EDGE_CURVE('',#1687,#1686,#1044,.T.);
#2133=EDGE_CURVE('',#1688,#1687,#1045,.T.);
#2134=EDGE_CURVE('',#1683,#1688,#1046,.T.);
#2135=EDGE_CURVE('',#1689,#1690,#1047,.T.);
#2136=EDGE_CURVE('',#1691,#1689,#1048,.T.);
#2137=EDGE_CURVE('',#1692,#1691,#1049,.T.);
#2138=EDGE_CURVE('',#1690,#1692,#1050,.T.);
#2139=EDGE_CURVE('',#1693,#1685,#1051,.T.);
#2140=EDGE_CURVE('',#1694,#1693,#1052,.T.);
#2141=EDGE_CURVE('',#1686,#1694,#1053,.T.);
#2142=EDGE_CURVE('',#1695,#1692,#784,.T.);
#2143=EDGE_CURVE('',#1695,#1696,#1054,.T.);
#2144=EDGE_CURVE('',#1690,#1696,#785,.T.);
#2145=EDGE_CURVE('',#1696,#1697,#1055,.T.);
#2146=EDGE_CURVE('',#1697,#1698,#786,.T.);
#2147=EDGE_CURVE('',#1698,#1699,#1056,.T.);
#2148=EDGE_CURVE('',#1699,#1700,#1057,.T.);
#2149=EDGE_CURVE('',#1700,#1701,#1058,.T.);
#2150=EDGE_CURVE('',#1701,#1702,#1059,.T.);
#2151=EDGE_CURVE('',#1702,#1693,#787,.T.);
#2152=EDGE_CURVE('',#1688,#1689,#1060,.T.);
#2153=EDGE_CURVE('',#1703,#1695,#1061,.T.);
#2154=EDGE_CURVE('',#1703,#1697,#1062,.T.);
#2155=EDGE_CURVE('',#1704,#1704,#788,.T.);
#2156=EDGE_CURVE('',#1705,#1699,#1063,.T.);
#2157=EDGE_CURVE('',#1706,#1698,#1064,.T.);
#2158=EDGE_CURVE('',#1706,#1707,#1065,.T.);
#2159=EDGE_CURVE('',#1707,#1708,#1066,.T.);
#2160=EDGE_CURVE('',#1705,#1708,#1067,.T.);
#2161=EDGE_CURVE('',#1709,#1710,#1068,.T.);
#2162=EDGE_CURVE('',#1710,#1706,#789,.T.);
#2163=EDGE_CURVE('',#1709,#1703,#790,.T.);
#2164=EDGE_CURVE('',#1711,#1712,#1069,.T.);
#2165=EDGE_CURVE('',#1711,#1713,#1070,.T.);
#2166=EDGE_CURVE('',#1713,#1714,#1071,.T.);
#2167=EDGE_CURVE('',#1712,#1714,#1072,.T.);
#2168=EDGE_CURVE('',#1707,#1713,#1073,.T.);
#2169=EDGE_CURVE('',#1708,#1711,#1074,.T.);
#2170=EDGE_CURVE('',#1714,#1710,#1075,.T.);
#2171=EDGE_CURVE('',#1712,#1709,#1076,.T.);
#2172=EDGE_CURVE('',#1702,#1715,#1077,.T.);
#2173=EDGE_CURVE('',#1694,#1715,#791,.T.);
#2174=EDGE_CURVE('',#1716,#1700,#1078,.T.);
#2175=EDGE_CURVE('',#1717,#1716,#1079,.T.);
#2176=EDGE_CURVE('',#1717,#1701,#1080,.T.);
#2177=EDGE_CURVE('',#1716,#1705,#1081,.T.);
#2178=EDGE_CURVE('',#1715,#1717,#1082,.T.);
#2179=EDGE_CURVE('',#1718,#1718,#792,.T.);
#2180=EDGE_CURVE('',#1718,#1704,#1083,.T.);
#2181=EDGE_CURVE('',#1691,#1687,#1084,.T.);
#2969=ORIENTED_EDGE('',*,*,#2119,.F.);
#2970=ORIENTED_EDGE('',*,*,#2120,.T.);
#2971=ORIENTED_EDGE('',*,*,#2121,.T.);
#2972=ORIENTED_EDGE('',*,*,#2122,.F.);
#2973=ORIENTED_EDGE('',*,*,#2123,.F.);
#2974=ORIENTED_EDGE('',*,*,#2124,.T.);
#2975=ORIENTED_EDGE('',*,*,#2125,.T.);
#2976=ORIENTED_EDGE('',*,*,#2120,.F.);
#2977=ORIENTED_EDGE('',*,*,#2126,.F.);
#2978=ORIENTED_EDGE('',*,*,#2127,.T.);
#2979=ORIENTED_EDGE('',*,*,#2128,.T.);
#2980=ORIENTED_EDGE('',*,*,#2124,.F.);
#2981=ORIENTED_EDGE('',*,*,#2129,.F.);
#2982=ORIENTED_EDGE('',*,*,#2121,.F.);
#2983=ORIENTED_EDGE('',*,*,#2125,.F.);
#2984=ORIENTED_EDGE('',*,*,#2128,.F.);
#2985=ORIENTED_EDGE('',*,*,#2126,.T.);
#2986=ORIENTED_EDGE('',*,*,#2123,.T.);
#2987=ORIENTED_EDGE('',*,*,#2119,.T.);
#2988=ORIENTED_EDGE('',*,*,#2130,.F.);
#2989=ORIENTED_EDGE('',*,*,#2131,.T.);
#2990=ORIENTED_EDGE('',*,*,#2132,.F.);
#2991=ORIENTED_EDGE('',*,*,#2133,.F.);
#2992=ORIENTED_EDGE('',*,*,#2134,.F.);
#2993=ORIENTED_EDGE('',*,*,#2135,.F.);
#2994=ORIENTED_EDGE('',*,*,#2136,.F.);
#2995=ORIENTED_EDGE('',*,*,#2137,.F.);
#2996=ORIENTED_EDGE('',*,*,#2138,.F.);
#2997=ORIENTED_EDGE('',*,*,#2139,.F.);
#2998=ORIENTED_EDGE('',*,*,#2140,.F.);
#2999=ORIENTED_EDGE('',*,*,#2141,.F.);
#3000=ORIENTED_EDGE('',*,*,#2131,.F.);
#3001=ORIENTED_EDGE('',*,*,#2138,.T.);
#3002=ORIENTED_EDGE('',*,*,#2142,.F.);
#3003=ORIENTED_EDGE('',*,*,#2143,.T.);
#3004=ORIENTED_EDGE('',*,*,#2144,.F.);
#3005=ORIENTED_EDGE('',*,*,#2135,.T.);
#3006=ORIENTED_EDGE('',*,*,#2144,.T.);
#3007=ORIENTED_EDGE('',*,*,#2145,.T.);
#3008=ORIENTED_EDGE('',*,*,#2146,.T.);
#3009=ORIENTED_EDGE('',*,*,#2147,.T.);
#3010=ORIENTED_EDGE('',*,*,#2148,.T.);
#3011=ORIENTED_EDGE('',*,*,#2149,.T.);
#3012=ORIENTED_EDGE('',*,*,#2150,.T.);
#3013=ORIENTED_EDGE('',*,*,#2151,.T.);
#3014=ORIENTED_EDGE('',*,*,#2139,.T.);
#3015=ORIENTED_EDGE('',*,*,#2130,.T.);
#3016=ORIENTED_EDGE('',*,*,#2122,.T.);
#3017=ORIENTED_EDGE('',*,*,#2129,.T.);
#3018=ORIENTED_EDGE('',*,*,#2127,.F.);
#3019=ORIENTED_EDGE('',*,*,#2134,.T.);
#3020=ORIENTED_EDGE('',*,*,#2152,.T.);
#3021=ORIENTED_EDGE('',*,*,#2153,.F.);
#3022=ORIENTED_EDGE('',*,*,#2154,.T.);
#3023=ORIENTED_EDGE('',*,*,#2145,.F.);
#3024=ORIENTED_EDGE('',*,*,#2143,.F.);
#3025=ORIENTED_EDGE('',*,*,#2155,.T.);
#3026=ORIENTED_EDGE('',*,*,#2156,.T.);
#3027=ORIENTED_EDGE('',*,*,#2147,.F.);
#3028=ORIENTED_EDGE('',*,*,#2157,.F.);
#3029=ORIENTED_EDGE('',*,*,#2158,.T.);
#3030=ORIENTED_EDGE('',*,*,#2159,.T.);
#3031=ORIENTED_EDGE('',*,*,#2160,.F.);
#3032=ORIENTED_EDGE('',*,*,#2161,.T.);
#3033=ORIENTED_EDGE('',*,*,#2162,.T.);
#3034=ORIENTED_EDGE('',*,*,#2157,.T.);
#3035=ORIENTED_EDGE('',*,*,#2146,.F.);
#3036=ORIENTED_EDGE('',*,*,#2154,.F.);
#3037=ORIENTED_EDGE('',*,*,#2163,.F.);
#3038=ORIENTED_EDGE('',*,*,#2164,.F.);
#3039=ORIENTED_EDGE('',*,*,#2165,.T.);
#3040=ORIENTED_EDGE('',*,*,#2166,.T.);
#3041=ORIENTED_EDGE('',*,*,#2167,.F.);
#3042=ORIENTED_EDGE('',*,*,#2159,.F.);
#3043=ORIENTED_EDGE('',*,*,#2168,.T.);
#3044=ORIENTED_EDGE('',*,*,#2165,.F.);
#3045=ORIENTED_EDGE('',*,*,#2169,.F.);
#3046=ORIENTED_EDGE('',*,*,#2162,.F.);
#3047=ORIENTED_EDGE('',*,*,#2170,.F.);
#3048=ORIENTED_EDGE('',*,*,#2166,.F.);
#3049=ORIENTED_EDGE('',*,*,#2168,.F.);
#3050=ORIENTED_EDGE('',*,*,#2158,.F.);
#3051=ORIENTED_EDGE('',*,*,#2161,.F.);
#3052=ORIENTED_EDGE('',*,*,#2171,.F.);
#3053=ORIENTED_EDGE('',*,*,#2167,.T.);
#3054=ORIENTED_EDGE('',*,*,#2170,.T.);
#3055=ORIENTED_EDGE('',*,*,#2140,.T.);
#3056=ORIENTED_EDGE('',*,*,#2151,.F.);
#3057=ORIENTED_EDGE('',*,*,#2172,.T.);
#3058=ORIENTED_EDGE('',*,*,#2173,.F.);
#3059=ORIENTED_EDGE('',*,*,#2149,.F.);
#3060=ORIENTED_EDGE('',*,*,#2174,.F.);
#3061=ORIENTED_EDGE('',*,*,#2175,.F.);
#3062=ORIENTED_EDGE('',*,*,#2176,.T.);
#3063=ORIENTED_EDGE('',*,*,#2148,.F.);
#3064=ORIENTED_EDGE('',*,*,#2156,.F.);
#3065=ORIENTED_EDGE('',*,*,#2177,.F.);
#3066=ORIENTED_EDGE('',*,*,#2174,.T.);
#3067=ORIENTED_EDGE('',*,*,#2150,.F.);
#3068=ORIENTED_EDGE('',*,*,#2176,.F.);
#3069=ORIENTED_EDGE('',*,*,#2178,.F.);
#3070=ORIENTED_EDGE('',*,*,#2172,.F.);
#3071=ORIENTED_EDGE('',*,*,#2179,.F.);
#3072=ORIENTED_EDGE('',*,*,#2180,.T.);
#3073=ORIENTED_EDGE('',*,*,#2155,.F.);
#3074=ORIENTED_EDGE('',*,*,#2180,.F.);
#3075=ORIENTED_EDGE('',*,*,#2136,.T.);
#3076=ORIENTED_EDGE('',*,*,#2152,.F.);
#3077=ORIENTED_EDGE('',*,*,#2133,.T.);
#3078=ORIENTED_EDGE('',*,*,#2181,.F.);
#3079=ORIENTED_EDGE('',*,*,#2179,.T.);
#3080=ORIENTED_EDGE('',*,*,#2137,.T.);
#3081=ORIENTED_EDGE('',*,*,#2181,.T.);
#3082=ORIENTED_EDGE('',*,*,#2132,.T.);
#3083=ORIENTED_EDGE('',*,*,#2141,.T.);
#3084=ORIENTED_EDGE('',*,*,#2173,.T.);
#3085=ORIENTED_EDGE('',*,*,#2178,.T.);
#3086=ORIENTED_EDGE('',*,*,#2175,.T.);
#3087=ORIENTED_EDGE('',*,*,#2177,.T.);
#3088=ORIENTED_EDGE('',*,*,#2160,.T.);
#3089=ORIENTED_EDGE('',*,*,#2169,.T.);
#3090=ORIENTED_EDGE('',*,*,#2164,.T.);
#3091=ORIENTED_EDGE('',*,*,#2171,.T.);
#3092=ORIENTED_EDGE('',*,*,#2163,.T.);
#3093=ORIENTED_EDGE('',*,*,#2153,.T.);
#3094=ORIENTED_EDGE('',*,*,#2142,.T.);
#3204=CYLINDRICAL_SURFACE('',#3835,4.99999999999999);
#3205=CYLINDRICAL_SURFACE('',#3844,4.99999999999999);
#3206=CYLINDRICAL_SURFACE('',#3851,4.99999999999999);
#3207=CYLINDRICAL_SURFACE('',#3856,2.5);
#3355=ADVANCED_FACE('',(#413),#229,.F.);
#3356=ADVANCED_FACE('',(#414),#230,.F.);
#3357=ADVANCED_FACE('',(#415),#231,.F.);
#3358=ADVANCED_FACE('',(#416),#232,.F.);
#3359=ADVANCED_FACE('',(#417),#233,.F.);
#3360=ADVANCED_FACE('',(#418),#234,.F.);
#3361=ADVANCED_FACE('',(#419),#235,.F.);
#3362=ADVANCED_FACE('',(#420),#3204,.F.);
#3363=ADVANCED_FACE('',(#421),#236,.F.);
#3364=ADVANCED_FACE('',(#422,#121),#237,.F.);
#3365=ADVANCED_FACE('',(#423),#238,.F.);
#3366=ADVANCED_FACE('',(#424),#3205,.F.);
#3367=ADVANCED_FACE('',(#425),#239,.F.);
#3368=ADVANCED_FACE('',(#426),#240,.F.);
#3369=ADVANCED_FACE('',(#427),#241,.F.);
#3370=ADVANCED_FACE('',(#428),#242,.F.);
#3371=ADVANCED_FACE('',(#429),#3206,.F.);
#3372=ADVANCED_FACE('',(#430),#243,.F.);
#3373=ADVANCED_FACE('',(#431),#244,.F.);
#3374=ADVANCED_FACE('',(#432),#245,.F.);
#3375=ADVANCED_FACE('',(#433),#3207,.F.);
#3376=ADVANCED_FACE('',(#434,#122),#246,.T.);
#3377=ADVANCED_FACE('',(#435),#247,.T.);
#3404=CLOSED_SHELL('',(#3355,#3356,#3357,#3358,#3359,#3360,#3361,#3362,
#3363,#3364,#3365,#3366,#3367,#3368,#3369,#3370,#3371,#3372,#3373,#3374,
#3375,#3376,#3377));
#3827=AXIS2_PLACEMENT_3D('',#5932,#4714,#4715);
#3828=AXIS2_PLACEMENT_3D('',#5933,#4716,#4717);
#3829=AXIS2_PLACEMENT_3D('',#5942,#4722,#4723);
#3830=AXIS2_PLACEMENT_3D('',#5948,#4727,#4728);
#3831=AXIS2_PLACEMENT_3D('',#5954,#4732,#4733);
#3832=AXIS2_PLACEMENT_3D('',#5956,#4735,#4736);
#3833=AXIS2_PLACEMENT_3D('',#5966,#4742,#4743);
#3834=AXIS2_PLACEMENT_3D('',#5975,#4748,#4749);
#3835=AXIS2_PLACEMENT_3D('',#5981,#4753,#4754);
#3836=AXIS2_PLACEMENT_3D('',#5983,#4755,#4756);
#3837=AXIS2_PLACEMENT_3D('',#5986,#4758,#4759);
#3838=AXIS2_PLACEMENT_3D('',#5987,#4760,#4761);
#3839=AXIS2_PLACEMENT_3D('',#5991,#4763,#4764);
#3840=AXIS2_PLACEMENT_3D('',#6000,#4769,#4770);
#3841=AXIS2_PLACEMENT_3D('',#6002,#4772,#4773);
#3842=AXIS2_PLACEMENT_3D('',#6007,#4776,#4777);
#3843=AXIS2_PLACEMENT_3D('',#6008,#4778,#4779);
#3844=AXIS2_PLACEMENT_3D('',#6018,#4785,#4786);
#3845=AXIS2_PLACEMENT_3D('',#6022,#4788,#4789);
#3846=AXIS2_PLACEMENT_3D('',#6023,#4790,#4791);
#3847=AXIS2_PLACEMENT_3D('',#6024,#4792,#4793);
#3848=AXIS2_PLACEMENT_3D('',#6033,#4798,#4799);
#3849=AXIS2_PLACEMENT_3D('',#6036,#4802,#4803);
#3850=AXIS2_PLACEMENT_3D('',#6038,#4805,#4806);
#3851=AXIS2_PLACEMENT_3D('',#6040,#4808,#4809);
#3852=AXIS2_PLACEMENT_3D('',#6043,#4811,#4812);
#3853=AXIS2_PLACEMENT_3D('',#6044,#4813,#4814);
#3854=AXIS2_PLACEMENT_3D('',#6050,#4818,#4819);
#3855=AXIS2_PLACEMENT_3D('',#6052,#4821,#4822);
#3856=AXIS2_PLACEMENT_3D('',#6054,#4824,#4825);
#3857=AXIS2_PLACEMENT_3D('',#6056,#4826,#4827);
#3858=AXIS2_PLACEMENT_3D('',#6058,#4829,#4830);
#3859=AXIS2_PLACEMENT_3D('',#6060,#4832,#4833);
#4714=DIRECTION('axis',(0.,0.,1.));
#4715=DIRECTION('refdir',(1.,0.,0.));
#4716=DIRECTION('center_axis',(0.,-1.,0.));
#4717=DIRECTION('ref_axis',(0.,0.,-1.));
#4718=DIRECTION('',(0.,0.,-1.));
#4719=DIRECTION('',(1.,0.,0.));
#4720=DIRECTION('',(0.,0.,-1.));
#4721=DIRECTION('',(1.,0.,0.));
#4722=DIRECTION('center_axis',(0.,0.,-1.));
#4723=DIRECTION('ref_axis',(0.,1.,0.));
#4724=DIRECTION('',(0.,1.,0.));
#4725=DIRECTION('',(1.,0.,0.));
#4726=DIRECTION('',(0.,1.,0.));
#4727=DIRECTION('center_axis',(0.,1.,0.));
#4728=DIRECTION('ref_axis',(0.,0.,1.));
#4729=DIRECTION('',(0.,0.,1.));
#4730=DIRECTION('',(1.,0.,0.));
#4731=DIRECTION('',(0.,0.,1.));
#4732=DIRECTION('center_axis',(-1.,0.,0.));
#4733=DIRECTION('ref_axis',(0.,0.,1.));
#4734=DIRECTION('',(0.,-1.,0.));
#4735=DIRECTION('center_axis',(-1.,0.,0.));
#4736=DIRECTION('ref_axis',(0.,1.,0.));
#4737=DIRECTION('',(0.,-1.,0.));
#4738=DIRECTION('',(0.,0.,1.));
#4739=DIRECTION('',(0.,1.,0.));
#4740=DIRECTION('',(0.,0.,1.));
#4741=DIRECTION('',(0.,-1.,0.));
#4742=DIRECTION('center_axis',(1.,0.,0.));
#4743=DIRECTION('ref_axis',(0.,-1.,0.));
#4744=DIRECTION('',(0.,1.,0.));
#4745=DIRECTION('',(0.,0.,-1.));
#4746=DIRECTION('',(0.,-1.,0.));
#4747=DIRECTION('',(0.,0.,1.));
#4748=DIRECTION('center_axis',(0.,-1.,0.));
#4749=DIRECTION('ref_axis',(-1.,0.,0.));
#4750=DIRECTION('',(1.,0.,0.));
#4751=DIRECTION('',(0.,0.,-1.));
#4752=DIRECTION('',(-1.,0.,0.));
#4753=DIRECTION('center_axis',(0.,0.,-1.));
#4754=DIRECTION('ref_axis',(-1.,8.88178419700126E-16,0.));
#4755=DIRECTION('center_axis',(0.,0.,-1.));
#4756=DIRECTION('ref_axis',(-1.,8.88178419700126E-16,0.));
#4757=DIRECTION('',(0.,0.,-1.));
#4758=DIRECTION('center_axis',(0.,0.,1.));
#4759=DIRECTION('ref_axis',(-1.,8.88178419700126E-16,0.));
#4760=DIRECTION('center_axis',(0.,0.,1.));
#4761=DIRECTION('ref_axis',(1.,0.,0.));
#4762=DIRECTION('',(1.,0.,0.));
#4763=DIRECTION('center_axis',(0.,0.,1.));
#4764=DIRECTION('ref_axis',(-1.33226762955019E-15,-1.,0.));
#4765=DIRECTION('',(0.,1.,0.));
#4766=DIRECTION('',(1.,0.,0.));
#4767=DIRECTION('',(0.,1.,0.));
#4768=DIRECTION('',(-1.,0.,0.));
#4769=DIRECTION('center_axis',(0.,0.,1.));
#4770=DIRECTION('ref_axis',(1.,-8.88178419700126E-16,0.));
#4771=DIRECTION('',(-1.,0.,0.));
#4772=DIRECTION('center_axis',(0.,-1.,0.));
#4773=DIRECTION('ref_axis',(-1.,0.,0.));
#4774=DIRECTION('',(-1.,0.,0.));
#4775=DIRECTION('',(0.,0.,-1.));
#4776=DIRECTION('center_axis',(0.,-1.,0.));
#4777=DIRECTION('ref_axis',(1.,0.,0.));
#4778=DIRECTION('center_axis',(1.,0.,0.));
#4779=DIRECTION('ref_axis',(0.,-1.,0.));
#4780=DIRECTION('',(0.,0.,-1.));
#4781=DIRECTION('',(0.,0.,-1.));
#4782=DIRECTION('',(0.,1.,0.));
#4783=DIRECTION('',(0.,0.,1.));
#4784=DIRECTION('',(0.,-1.,0.));
#4785=DIRECTION('center_axis',(0.,0.,-1.));
#4786=DIRECTION('ref_axis',(-1.33226762955019E-15,-1.,0.));
#4787=DIRECTION('',(0.,0.,-1.));
#4788=DIRECTION('center_axis',(0.,0.,1.));
#4789=DIRECTION('ref_axis',(-1.33226762955019E-15,-1.,0.));
#4790=DIRECTION('center_axis',(0.,0.,-1.));
#4791=DIRECTION('ref_axis',(-1.33226762955019E-15,-1.,0.));
#4792=DIRECTION('center_axis',(1.,0.,0.));
#4793=DIRECTION('ref_axis',(0.,-1.,0.));
#4794=DIRECTION('',(0.,-1.,0.));
#4795=DIRECTION('',(0.,0.,-1.));
#4796=DIRECTION('',(0.,-1.,0.));
#4797=DIRECTION('',(0.,0.,-1.));
#4798=DIRECTION('center_axis',(0.,1.,0.));
#4799=DIRECTION('ref_axis',(1.,0.,0.));
#4800=DIRECTION('',(1.,0.,0.));
#4801=DIRECTION('',(1.,0.,0.));
#4802=DIRECTION('center_axis',(0.,0.,-1.));
#4803=DIRECTION('ref_axis',(-1.,0.,0.));
#4804=DIRECTION('',(-1.,0.,0.));
#4805=DIRECTION('center_axis',(0.,-1.,0.));
#4806=DIRECTION('ref_axis',(-1.,0.,0.));
#4807=DIRECTION('',(-1.,0.,0.));
#4808=DIRECTION('center_axis',(0.,0.,-1.));
#4809=DIRECTION('ref_axis',(1.,-8.88178419700126E-16,0.));
#4810=DIRECTION('',(0.,0.,1.));
#4811=DIRECTION('center_axis',(0.,0.,-1.));
#4812=DIRECTION('ref_axis',(1.,-8.88178419700126E-16,0.));
#4813=DIRECTION('center_axis',(1.,0.,0.));
#4814=DIRECTION('ref_axis',(0.,-1.,0.));
#4815=DIRECTION('',(0.,0.,-1.));
#4816=DIRECTION('',(0.,-1.,0.));
#4817=DIRECTION('',(0.,0.,-1.));
#4818=DIRECTION('center_axis',(0.,-1.,0.));
#4819=DIRECTION('ref_axis',(-1.,0.,0.));
#4820=DIRECTION('',(-1.,0.,0.));
#4821=DIRECTION('center_axis',(0.,1.,0.));
#4822=DIRECTION('ref_axis',(1.,0.,0.));
#4823=DIRECTION('',(1.,0.,0.));
#4824=DIRECTION('center_axis',(0.,1.,0.));
#4825=DIRECTION('ref_axis',(1.,0.,0.));
#4826=DIRECTION('center_axis',(0.,1.,0.));
#4827=DIRECTION('ref_axis',(1.,0.,0.));
#4828=DIRECTION('',(0.,1.,0.));
#4829=DIRECTION('center_axis',(0.,-1.,0.));
#4830=DIRECTION('ref_axis',(1.,0.,0.));
#4831=DIRECTION('',(1.,0.,0.));
#4832=DIRECTION('center_axis',(0.,0.,1.));
#4833=DIRECTION('ref_axis',(1.,0.,0.));
#5932=CARTESIAN_POINT('',(0.,0.,0.));
#5933=CARTESIAN_POINT('Origin',(29.1374542444053,4.,6.));
#5934=CARTESIAN_POINT('',(29.1374542444053,4.,6.));
#5935=CARTESIAN_POINT('',(29.1374542444053,4.,0.));
#5936=CARTESIAN_POINT('',(29.1374542444053,4.,11.));
#5937=CARTESIAN_POINT('',(35.1374542444053,4.,6.));
#5938=CARTESIAN_POINT('',(29.1374542444053,4.,6.));
#5939=CARTESIAN_POINT('',(35.1374542444053,4.,0.));
#5940=CARTESIAN_POINT('',(35.1374542444053,4.,6.));
#5941=CARTESIAN_POINT('',(29.1374542444053,4.,0.));
#5942=CARTESIAN_POINT('Origin',(29.1374542444053,-4.,6.));
#5943=CARTESIAN_POINT('',(29.1374542444053,-4.,6.));
#5944=CARTESIAN_POINT('',(29.1374542444053,-17.,6.));
#5945=CARTESIAN_POINT('',(35.1374542444053,-4.,6.));
#5946=CARTESIAN_POINT('',(29.1374542444053,-4.,6.));
#5947=CARTESIAN_POINT('',(35.1374542444053,-4.,6.));
#5948=CARTESIAN_POINT('Origin',(29.1374542444053,-4.,0.));
#5949=CARTESIAN_POINT('',(29.1374542444053,-4.,0.));
#5950=CARTESIAN_POINT('',(29.1374542444053,-4.,8.));
#5951=CARTESIAN_POINT('',(35.1374542444053,-4.,0.));
#5952=CARTESIAN_POINT('',(29.1374542444053,-4.,0.));
#5953=CARTESIAN_POINT('',(35.1374542444053,-4.,-6.));
#5954=CARTESIAN_POINT('Origin',(35.1374542444053,0.,3.));
#5955=CARTESIAN_POINT('',(35.1374542444053,30.,0.));
#5956=CARTESIAN_POINT('Origin',(29.1374542444053,-30.,16.));
#5957=CARTESIAN_POINT('',(29.1374542444053,14.5,0.));
#5958=CARTESIAN_POINT('',(29.1374542444053,-15.,0.));
#5959=CARTESIAN_POINT('',(29.1374542444053,14.5,16.));
#5960=CARTESIAN_POINT('',(29.1374542444053,14.5,16.));
#5961=CARTESIAN_POINT('',(29.1374542444053,-30.,16.));
#5962=CARTESIAN_POINT('',(29.1374542444053,-15.,16.));
#5963=CARTESIAN_POINT('',(29.1374542444053,-30.,0.));
#5964=CARTESIAN_POINT('',(29.1374542444053,-30.,8.));
#5965=CARTESIAN_POINT('',(29.1374542444053,-15.,0.));
#5966=CARTESIAN_POINT('Origin',(-19.0332022605826,-12.9552122639891,16.));
#5967=CARTESIAN_POINT('',(-19.0332022605826,-30.,0.));
#5968=CARTESIAN_POINT('',(-19.0332022605826,-12.9552122639891,0.));
#5969=CARTESIAN_POINT('',(-19.0332022605826,-6.47760613199456,0.));
#5970=CARTESIAN_POINT('',(-19.0332022605826,-30.,16.));
#5971=CARTESIAN_POINT('',(-19.0332022605826,-30.,8.));
#5972=CARTESIAN_POINT('',(-19.0332022605826,-12.9552122639891,16.));
#5973=CARTESIAN_POINT('',(-19.0332022605826,-6.47760613199456,16.));
#5974=CARTESIAN_POINT('',(-19.0332022605826,-12.9552122639891,16.));
#5975=CARTESIAN_POINT('Origin',(29.1374542444053,14.5,16.));
#5976=CARTESIAN_POINT('',(17.1794494717703,14.5,0.));
#5977=CARTESIAN_POINT('',(14.5687271222026,14.5,0.));
#5978=CARTESIAN_POINT('',(17.1794494717703,14.5,16.));
#5979=CARTESIAN_POINT('',(17.1794494717703,14.5,16.));
#5980=CARTESIAN_POINT('',(14.5687271222026,14.5,16.));
#5981=CARTESIAN_POINT('Origin',(-15.,-10.,16.));
#5982=CARTESIAN_POINT('',(-15.,-15.,16.));
#5983=CARTESIAN_POINT('Origin',(-15.,-10.,16.));
#5984=CARTESIAN_POINT('',(-15.,-15.,0.));
#5985=CARTESIAN_POINT('',(-15.,-15.,16.));
#5986=CARTESIAN_POINT('Origin',(-15.,-10.,0.));
#5987=CARTESIAN_POINT('Origin',(0.,0.,0.));
#5988=CARTESIAN_POINT('',(15.,-15.,0.));
#5989=CARTESIAN_POINT('',(7.5,-15.,0.));
#5990=CARTESIAN_POINT('',(20.,-10.,0.));
#5991=CARTESIAN_POINT('Origin',(15.,-10.,0.));
#5992=CARTESIAN_POINT('',(20.,8.18152526714698,0.));
#5993=CARTESIAN_POINT('',(20.,5.,0.));
#5994=CARTESIAN_POINT('',(21.,8.18152526714698,0.));
#5995=CARTESIAN_POINT('',(10.5,8.18152526714698,0.));
#5996=CARTESIAN_POINT('',(21.,12.8450798069859,0.));
#5997=CARTESIAN_POINT('',(21.,6.42253990349293,0.));
#5998=CARTESIAN_POINT('',(19.1116323877362,12.8450798069859,0.));
#5999=CARTESIAN_POINT('',(9.00717937525703,12.8450798069859,0.));
#6000=CARTESIAN_POINT('Origin',(15.,10.,0.));
#6001=CARTESIAN_POINT('',(50.,-30.,0.));
#6002=CARTESIAN_POINT('Origin',(15.,-15.,16.));
#6003=CARTESIAN_POINT('',(15.,-15.,16.));
#6004=CARTESIAN_POINT('',(7.5,-15.,16.));
#6005=CARTESIAN_POINT('',(15.,-15.,16.));
#6006=CARTESIAN_POINT('',(-14.1523566026163,-15.,8.));
#6007=CARTESIAN_POINT('Origin',(-11.6523566026163,-15.,8.));
#6008=CARTESIAN_POINT('Origin',(20.,10.,16.));
#6009=CARTESIAN_POINT('',(20.,8.18152526714698,16.));
#6010=CARTESIAN_POINT('',(20.,8.18152526714698,16.));
#6011=CARTESIAN_POINT('',(20.,-10.,14.));
#6012=CARTESIAN_POINT('',(20.,-10.,16.));
#6013=CARTESIAN_POINT('',(20.,-2.10952062437159,14.));
#6014=CARTESIAN_POINT('',(20.,1.44523968781421,14.));
#6015=CARTESIAN_POINT('',(20.,-2.10952062437159,16.));
#6016=CARTESIAN_POINT('',(20.,-2.10952062437159,16.));
#6017=CARTESIAN_POINT('',(20.,5.,16.));
#6018=CARTESIAN_POINT('Origin',(15.,-10.,16.));
#6019=CARTESIAN_POINT('',(19.5332022605826,-12.1095206243716,16.));
#6020=CARTESIAN_POINT('',(19.5332022605826,-12.1095206243716,14.));
#6021=CARTESIAN_POINT('',(19.5332022605826,-12.1095206243716,16.));
#6022=CARTESIAN_POINT('Origin',(15.,-10.,14.));
#6023=CARTESIAN_POINT('Origin',(15.,-10.,16.));
#6024=CARTESIAN_POINT('Origin',(25.,-2.10952062437159,16.));
#6025=CARTESIAN_POINT('',(25.,-2.10952062437159,16.));
#6026=CARTESIAN_POINT('',(25.,-12.1095206243716,16.));
#6027=CARTESIAN_POINT('',(25.,-1.0547603121858,16.));
#6028=CARTESIAN_POINT('',(25.,-2.10952062437159,14.));
#6029=CARTESIAN_POINT('',(25.,-2.10952062437159,16.));
#6030=CARTESIAN_POINT('',(25.,-12.1095206243716,14.));
#6031=CARTESIAN_POINT('',(25.,-12.1095206243716,14.));
#6032=CARTESIAN_POINT('',(25.,-12.1095206243716,16.));
#6033=CARTESIAN_POINT('Origin',(-25.,-2.10952062437159,16.));
#6034=CARTESIAN_POINT('',(25.,-2.10952062437159,14.));
#6035=CARTESIAN_POINT('',(-12.5,-2.10952062437159,16.));
#6036=CARTESIAN_POINT('Origin',(0.,-7.10952062437159,14.));
#6037=CARTESIAN_POINT('',(-25.,-12.1095206243716,14.));
#6038=CARTESIAN_POINT('Origin',(25.,-12.1095206243716,16.));
#6039=CARTESIAN_POINT('',(12.5,-12.1095206243716,16.));
#6040=CARTESIAN_POINT('Origin',(15.,10.,16.));
#6041=CARTESIAN_POINT('',(19.1116323877362,12.8450798069859,16.));
#6042=CARTESIAN_POINT('',(19.1116323877362,12.8450798069859,16.));
#6043=CARTESIAN_POINT('Origin',(15.,10.,16.));
#6044=CARTESIAN_POINT('Origin',(21.,12.8450798069859,16.));
#6045=CARTESIAN_POINT('',(21.,8.18152526714698,16.));
#6046=CARTESIAN_POINT('',(21.,8.18152526714698,16.));
#6047=CARTESIAN_POINT('',(21.,12.8450798069859,16.));
#6048=CARTESIAN_POINT('',(21.,6.42253990349293,16.));
#6049=CARTESIAN_POINT('',(21.,12.8450798069859,16.));
#6050=CARTESIAN_POINT('Origin',(21.,8.18152526714698,16.));
#6051=CARTESIAN_POINT('',(10.5,8.18152526714698,16.));
#6052=CARTESIAN_POINT('Origin',(18.0143587505141,12.8450798069859,16.));
#6053=CARTESIAN_POINT('',(9.00717937525703,12.8450798069859,16.));
#6054=CARTESIAN_POINT('Origin',(-11.6523566026163,-30.,8.));
#6055=CARTESIAN_POINT('',(-14.1523566026163,-30.,8.));
#6056=CARTESIAN_POINT('Origin',(-11.6523566026163,-30.,8.));
#6057=CARTESIAN_POINT('',(-14.1523566026163,-30.,8.));
#6058=CARTESIAN_POINT('Origin',(-50.,-30.,0.));
#6059=CARTESIAN_POINT('',(50.,-30.,16.));
#6060=CARTESIAN_POINT('Origin',(0.,0.,16.));
#7032=UNCERTAINTY_MEASURE_WITH_UNIT(LENGTH_MEASURE(0.01),#7048,
'DISTANCE_ACCURACY_VALUE',
'Maximum model space distance between geometric entities at asserted c
onnectivities');
#7035=UNCERTAINTY_MEASURE_WITH_UNIT(LENGTH_MEASURE(0.01),#7048,
'DISTANCE_ACCURACY_VALUE',
'Maximum model space distance between geometric entities at asserted c
onnectivities');
#7044=(
GEOMETRIC_REPRESENTATION_CONTEXT(3)
GLOBAL_UNCERTAINTY_ASSIGNED_CONTEXT((#7032))
GLOBAL_UNIT_ASSIGNED_CONTEXT((#7048,#7050,#7051))
REPRESENTATION_CONTEXT('','3D')
);
#7047=(
GEOMETRIC_REPRESENTATION_CONTEXT(3)
GLOBAL_UNCERTAINTY_ASSIGNED_CONTEXT((#7035))
GLOBAL_UNIT_ASSIGNED_CONTEXT((#7048,#7050,#7051))
REPRESENTATION_CONTEXT('','3D')
);
#7048=(
LENGTH_UNIT()
NAMED_UNIT(*)
SI_UNIT(.MILLI.,.METRE.)
);
#7050=(
NAMED_UNIT(*)
PLANE_ANGLE_UNIT()
SI_UNIT($,.RADIAN.)
);
#7051=(
NAMED_UNIT(*)
SI_UNIT($,.STERADIAN.)
SOLID_ANGLE_UNIT()
);
#7060=SHAPE_DEFINITION_REPRESENTATION(#7071,#7092);
#7071=PRODUCT_DEFINITION_SHAPE('',$,#7104);
#7092=SHAPE_REPRESENTATION('',(#3827),#7044);
#7095=PRODUCT_DEFINITION_CONTEXT('part definition',#7130,'design');
#7104=PRODUCT_DEFINITION('Right_Block','Right_Block',#7115,#7095);
#7115=PRODUCT_DEFINITION_FORMATION('',$,#7140);
#7130=APPLICATION_CONTEXT(
'Core Data for Automotive Mechanical Design Process');
#7131=PRODUCT_CONTEXT('part definition',#7130,'mechanical');
#7140=PRODUCT('Right_Block','Right_Block',$,(#7131));
#7171=COLOUR_RGB('Dark Blue',0.08,0.2,0.34);
#7172=FILL_AREA_STYLE_COLOUR('',#7171);
#7173=FILL_AREA_STYLE('',(#7172));
#7174=SURFACE_STYLE_FILL_AREA(#7173);
#7175=SURFACE_SIDE_STYLE('',(#7174));
#7176=SURFACE_STYLE_USAGE(.BOTH.,#7175);
#7177=PRESENTATION_STYLE_ASSIGNMENT((#7176));
ENDSEC;
END-ISO-10303-21;
